ISO-10303-21;
HEADER;
/* Generated by software containing ST-Developer
 * from STEP Tools, Inc. (www.steptools.com) 
 */
/* OPTION: using custom renumber hook */

FILE_DESCRIPTION(
/* description */ ('STEP AP242 Edition 2', 'CAx-IF Rec.Pracs.---Representation and Presentation of Product Manufa
cturing Information (PMI)---4.0---2014-10-13', 'CAx-IF Rec.Pracs.---3D Tessellated Geometry---0.4---2014-09-14', '2;1', 'CAx-IF Rec.Pracs.---User Defined Attributes---1.5---2016-08-15'),
/* implementation_level */ '2;1');

FILE_NAME(
/* name */ 'Part 1__PD10224.step',
/* time_stamp */ '2026-10-09T13:59:33Z',
/* author */ (''),
/* organization */ (''),
/* preprocessor_version */ 'ST-DEVELOPER v20',
/* originating_system */ 'ONSHAPE BY PTC INC, 1.221',
/* authorisation */ '  ');

FILE_SCHEMA (('AP242_MANAGED_MODEL_BASED_3D_ENGINEERING_MIM_LF { 1 0 10303 442 3 1 4 }'));
ENDSEC;

DATA;
#294=LINE('',#9995,#578);
#295=LINE('',#9999,#579);
#296=LINE('',#10001,#580);
#297=LINE('',#10005,#581);
#298=LINE('',#10011,#582);
#299=LINE('',#10018,#583);
#300=LINE('',#10024,#584);
#301=LINE('',#10028,#585);
#302=LINE('',#10030,#586);
#303=LINE('',#10034,#587);
#304=LINE('',#10040,#588);
#305=LINE('',#10041,#589);
#306=LINE('',#10043,#590);
#307=LINE('',#10045,#591);
#308=LINE('',#10047,#592);
#309=LINE('',#10049,#593);
#310=LINE('',#10051,#594);
#311=LINE('',#10053,#595);
#312=LINE('',#10055,#596);
#313=LINE('',#10057,#597);
#314=LINE('',#10059,#598);
#578=VECTOR('',#8264,1.);
#579=VECTOR('',#8267,1.);
#580=VECTOR('',#8268,1.);
#581=VECTOR('',#8271,1.);
#582=VECTOR('',#8276,1.);
#583=VECTOR('',#8283,1.);
#584=VECTOR('',#8288,1.);
#585=VECTOR('',#8291,1.);
#586=VECTOR('',#8292,1.);
#587=VECTOR('',#8295,1.);
#588=VECTOR('',#8302,1.);
#589=VECTOR('',#8303,1.);
#590=VECTOR('',#8306,1.);
#591=VECTOR('',#8309,1.);
#592=VECTOR('',#8312,1.);
#593=VECTOR('',#8315,1.);
#594=VECTOR('',#8318,1.);
#595=VECTOR('',#8321,1.);
#596=VECTOR('',#8324,1.);
#597=VECTOR('',#8327,1.);
#598=VECTOR('',#8330,1.);
#683=SHAPE_REPRESENTATION_RELATIONSHIP('','',#5702,#697);
#697=ADVANCED_BREP_SHAPE_REPRESENTATION('',(#5670),#10156);
#776=PLANE('',#6451);
#777=PLANE('',#6459);
#778=PLANE('',#6469);
#779=PLANE('',#6471);
#780=PLANE('',#6472);
#781=PLANE('',#6474);
#782=PLANE('',#6477);
#2228=ORIENTED_EDGE('',*,*,#3051,.T.);
#2229=ORIENTED_EDGE('',*,*,#3052,.T.);
#2230=ORIENTED_EDGE('',*,*,#3053,.T.);
#2231=ORIENTED_EDGE('',*,*,#3054,.T.);
#2232=ORIENTED_EDGE('',*,*,#3055,.T.);
#2233=ORIENTED_EDGE('',*,*,#3056,.T.);
#2234=ORIENTED_EDGE('',*,*,#3057,.T.);
#2235=ORIENTED_EDGE('',*,*,#3058,.T.);
#2236=ORIENTED_EDGE('',*,*,#3059,.T.);
#2237=ORIENTED_EDGE('',*,*,#3060,.T.);
#2238=ORIENTED_EDGE('',*,*,#3061,.T.);
#2239=ORIENTED_EDGE('',*,*,#3062,.F.);
#2240=ORIENTED_EDGE('',*,*,#3063,.F.);
#2241=ORIENTED_EDGE('',*,*,#3064,.F.);
#2242=ORIENTED_EDGE('',*,*,#3065,.F.);
#2243=ORIENTED_EDGE('',*,*,#3066,.F.);
#2244=ORIENTED_EDGE('',*,*,#3067,.F.);
#2245=ORIENTED_EDGE('',*,*,#3068,.F.);
#2246=ORIENTED_EDGE('',*,*,#3069,.F.);
#2247=ORIENTED_EDGE('',*,*,#3070,.F.);
#2248=ORIENTED_EDGE('',*,*,#3071,.F.);
#2249=ORIENTED_EDGE('',*,*,#3072,.F.);
#2250=ORIENTED_EDGE('',*,*,#3073,.F.);
#2251=ORIENTED_EDGE('',*,*,#3074,.T.);
#2252=ORIENTED_EDGE('',*,*,#3063,.T.);
#2253=ORIENTED_EDGE('',*,*,#3075,.F.);
#2254=ORIENTED_EDGE('',*,*,#3051,.F.);
#2255=ORIENTED_EDGE('',*,*,#3076,.T.);
#2256=ORIENTED_EDGE('',*,*,#3073,.T.);
#2257=ORIENTED_EDGE('',*,*,#3077,.F.);
#2258=ORIENTED_EDGE('',*,*,#3052,.F.);
#2259=ORIENTED_EDGE('',*,*,#3075,.T.);
#2260=ORIENTED_EDGE('',*,*,#3072,.T.);
#2261=ORIENTED_EDGE('',*,*,#3078,.F.);
#2262=ORIENTED_EDGE('',*,*,#3053,.F.);
#2263=ORIENTED_EDGE('',*,*,#3077,.T.);
#2264=ORIENTED_EDGE('',*,*,#3071,.T.);
#2265=ORIENTED_EDGE('',*,*,#3079,.F.);
#2266=ORIENTED_EDGE('',*,*,#3054,.F.);
#2267=ORIENTED_EDGE('',*,*,#3078,.T.);
#2268=ORIENTED_EDGE('',*,*,#3070,.T.);
#2269=ORIENTED_EDGE('',*,*,#3080,.F.);
#2270=ORIENTED_EDGE('',*,*,#3055,.F.);
#2271=ORIENTED_EDGE('',*,*,#3079,.T.);
#2272=ORIENTED_EDGE('',*,*,#3069,.T.);
#2273=ORIENTED_EDGE('',*,*,#3081,.F.);
#2274=ORIENTED_EDGE('',*,*,#3056,.F.);
#2275=ORIENTED_EDGE('',*,*,#3080,.T.);
#2276=ORIENTED_EDGE('',*,*,#3068,.T.);
#2277=ORIENTED_EDGE('',*,*,#3082,.F.);
#2278=ORIENTED_EDGE('',*,*,#3057,.F.);
#2279=ORIENTED_EDGE('',*,*,#3081,.T.);
#2280=ORIENTED_EDGE('',*,*,#3067,.T.);
#2281=ORIENTED_EDGE('',*,*,#3083,.F.);
#2282=ORIENTED_EDGE('',*,*,#3058,.F.);
#2283=ORIENTED_EDGE('',*,*,#3082,.T.);
#2284=ORIENTED_EDGE('',*,*,#3066,.T.);
#2285=ORIENTED_EDGE('',*,*,#3084,.F.);
#2286=ORIENTED_EDGE('',*,*,#3059,.F.);
#2287=ORIENTED_EDGE('',*,*,#3083,.T.);
#2288=ORIENTED_EDGE('',*,*,#3065,.T.);
#2289=ORIENTED_EDGE('',*,*,#3085,.F.);
#2290=ORIENTED_EDGE('',*,*,#3060,.F.);
#2291=ORIENTED_EDGE('',*,*,#3084,.T.);
#2292=ORIENTED_EDGE('',*,*,#3064,.T.);
#2293=ORIENTED_EDGE('',*,*,#3076,.F.);
#2294=ORIENTED_EDGE('',*,*,#3061,.F.);
#2295=ORIENTED_EDGE('',*,*,#3085,.T.);
#2296=ORIENTED_EDGE('',*,*,#3062,.T.);
#2297=ORIENTED_EDGE('',*,*,#3074,.F.);
#3051=EDGE_CURVE('',#3609,#3610,#4082,.T.);
#3052=EDGE_CURVE('',#3610,#3611,#4083,.T.);
#3053=EDGE_CURVE('',#3611,#3612,#294,.T.);
#3054=EDGE_CURVE('',#3612,#3613,#4084,.T.);
#3055=EDGE_CURVE('',#3613,#3614,#295,.T.);
#3056=EDGE_CURVE('',#3614,#3615,#296,.T.);
#3057=EDGE_CURVE('',#3615,#3616,#4085,.T.);
#3058=EDGE_CURVE('',#3616,#3617,#297,.T.);
#3059=EDGE_CURVE('',#3617,#3618,#4086,.T.);
#3060=EDGE_CURVE('',#3618,#3619,#4087,.T.);
#3061=EDGE_CURVE('',#3619,#3609,#298,.T.);
#3062=EDGE_CURVE('',#3620,#3620,#4088,.T.);
#3063=EDGE_CURVE('',#3621,#3622,#4089,.T.);
#3064=EDGE_CURVE('',#3623,#3621,#299,.T.);
#3065=EDGE_CURVE('',#3624,#3623,#4090,.T.);
#3066=EDGE_CURVE('',#3625,#3624,#4091,.T.);
#3067=EDGE_CURVE('',#3626,#3625,#300,.T.);
#3068=EDGE_CURVE('',#3627,#3626,#4092,.T.);
#3069=EDGE_CURVE('',#3628,#3627,#301,.T.);
#3070=EDGE_CURVE('',#3629,#3628,#302,.T.);
#3071=EDGE_CURVE('',#3630,#3629,#4093,.T.);
#3072=EDGE_CURVE('',#3631,#3630,#303,.T.);
#3073=EDGE_CURVE('',#3622,#3631,#4094,.T.);
#3074=EDGE_CURVE('',#3632,#3632,#4095,.T.);
#3075=EDGE_CURVE('',#3610,#3622,#304,.T.);
#3076=EDGE_CURVE('',#3609,#3621,#305,.T.);
#3077=EDGE_CURVE('',#3611,#3631,#306,.T.);
#3078=EDGE_CURVE('',#3612,#3630,#307,.T.);
#3079=EDGE_CURVE('',#3613,#3629,#308,.T.);
#3080=EDGE_CURVE('',#3614,#3628,#309,.T.);
#3081=EDGE_CURVE('',#3615,#3627,#310,.T.);
#3082=EDGE_CURVE('',#3616,#3626,#311,.T.);
#3083=EDGE_CURVE('',#3617,#3625,#312,.T.);
#3084=EDGE_CURVE('',#3618,#3624,#313,.T.);
#3085=EDGE_CURVE('',#3619,#3623,#314,.T.);
#3609=VERTEX_POINT('',#9991);
#3610=VERTEX_POINT('',#9992);
#3611=VERTEX_POINT('',#9994);
#3612=VERTEX_POINT('',#9996);
#3613=VERTEX_POINT('',#9998);
#3614=VERTEX_POINT('',#10000);
#3615=VERTEX_POINT('',#10002);
#3616=VERTEX_POINT('',#10004);
#3617=VERTEX_POINT('',#10006);
#3618=VERTEX_POINT('',#10008);
#3619=VERTEX_POINT('',#10010);
#3620=VERTEX_POINT('',#10013);
#3621=VERTEX_POINT('',#10016);
#3622=VERTEX_POINT('',#10017);
#3623=VERTEX_POINT('',#10019);
#3624=VERTEX_POINT('',#10021);
#3625=VERTEX_POINT('',#10023);
#3626=VERTEX_POINT('',#10025);
#3627=VERTEX_POINT('',#10027);
#3628=VERTEX_POINT('',#10029);
#3629=VERTEX_POINT('',#10031);
#3630=VERTEX_POINT('',#10033);
#3631=VERTEX_POINT('',#10035);
#3632=VERTEX_POINT('',#10038);
#4082=CIRCLE('',#6452,0.000257682665739803);
#4083=CIRCLE('',#6453,0.00755256285496241);
#4084=CIRCLE('',#6454,0.0025);
#4085=CIRCLE('',#6455,0.0025);
#4086=CIRCLE('',#6456,0.00755256285496241);
#4087=CIRCLE('',#6457,0.000257682665739803);
#4088=CIRCLE('',#6458,0.0015);
#4089=CIRCLE('',#6460,0.000257682665739803);
#4090=CIRCLE('',#6461,0.000257682665739803);
#4091=CIRCLE('',#6462,0.00755256285496241);
#4092=CIRCLE('',#6463,0.0025);
#4093=CIRCLE('',#6464,0.0025);
#4094=CIRCLE('',#6465,0.00755256285496241);
#4095=CIRCLE('',#6466,0.0015);
#4520=EDGE_LOOP('',(#2228,#2229,#2230,#2231,#2232,#2233,#2234,#2235,#2236,
#2237,#2238));
#4521=EDGE_LOOP('',(#2239));
#4522=EDGE_LOOP('',(#2240,#2241,#2242,#2243,#2244,#2245,#2246,#2247,#2248,
#2249,#2250));
#4523=EDGE_LOOP('',(#2251));
#4524=EDGE_LOOP('',(#2252,#2253,#2254,#2255));
#4525=EDGE_LOOP('',(#2256,#2257,#2258,#2259));
#4526=EDGE_LOOP('',(#2260,#2261,#2262,#2263));
#4527=EDGE_LOOP('',(#2264,#2265,#2266,#2267));
#4528=EDGE_LOOP('',(#2268,#2269,#2270,#2271));
#4529=EDGE_LOOP('',(#2272,#2273,#2274,#2275));
#4530=EDGE_LOOP('',(#2276,#2277,#2278,#2279));
#4531=EDGE_LOOP('',(#2280,#2281,#2282,#2283));
#4532=EDGE_LOOP('',(#2284,#2285,#2286,#2287));
#4533=EDGE_LOOP('',(#2288,#2289,#2290,#2291));
#4534=EDGE_LOOP('',(#2292,#2293,#2294,#2295));
#4535=EDGE_LOOP('',(#2296));
#4536=EDGE_LOOP('',(#2297));
#4968=FACE_BOUND('',#4520,.T.);
#4969=FACE_BOUND('',#4521,.T.);
#4970=FACE_BOUND('',#4522,.T.);
#4971=FACE_BOUND('',#4523,.T.);
#4972=FACE_BOUND('',#4524,.T.);
#4973=FACE_BOUND('',#4525,.T.);
#4974=FACE_BOUND('',#4526,.T.);
#4975=FACE_BOUND('',#4527,.T.);
#4976=FACE_BOUND('',#4528,.T.);
#4977=FACE_BOUND('',#4529,.T.);
#4978=FACE_BOUND('',#4530,.T.);
#4979=FACE_BOUND('',#4531,.T.);
#4980=FACE_BOUND('',#4532,.T.);
#4981=FACE_BOUND('',#4533,.T.);
#4982=FACE_BOUND('',#4534,.T.);
#4983=FACE_BOUND('',#4535,.T.);
#4984=FACE_BOUND('',#4536,.T.);
#5205=CYLINDRICAL_SURFACE('',#6467,0.000257682665739803);
#5206=CYLINDRICAL_SURFACE('',#6468,0.00755256285496241);
#5207=CYLINDRICAL_SURFACE('',#6470,0.0025);
#5208=CYLINDRICAL_SURFACE('',#6473,0.0025);
#5209=CYLINDRICAL_SURFACE('',#6475,0.00755256285496241);
#5210=CYLINDRICAL_SURFACE('',#6476,0.000257682665739803);
#5211=CYLINDRICAL_SURFACE('',#6478,0.0015);
#5512=ADVANCED_FACE('',(#4968,#4969),#776,.T.);
#5513=ADVANCED_FACE('',(#4970,#4971),#777,.F.);
#5514=ADVANCED_FACE('',(#4972),#5205,.T.);
#5515=ADVANCED_FACE('',(#4973),#5206,.F.);
#5516=ADVANCED_FACE('',(#4974),#778,.F.);
#5517=ADVANCED_FACE('',(#4975),#5207,.T.);
#5518=ADVANCED_FACE('',(#4976),#779,.F.);
#5519=ADVANCED_FACE('',(#4977),#780,.F.);
#5520=ADVANCED_FACE('',(#4978),#5208,.T.);
#5521=ADVANCED_FACE('',(#4979),#781,.F.);
#5522=ADVANCED_FACE('',(#4980),#5209,.F.);
#5523=ADVANCED_FACE('',(#4981),#5210,.T.);
#5524=ADVANCED_FACE('',(#4982),#782,.F.);
#5525=ADVANCED_FACE('',(#4983,#4984),#5211,.F.);
#5551=CLOSED_SHELL('',(#5512,#5513,#5514,#5515,#5516,#5517,#5518,#5519,
#5520,#5521,#5522,#5523,#5524,#5525));
#5565=STYLED_ITEM('',(#5579),#5670);
#5579=PRESENTATION_STYLE_ASSIGNMENT((#5593));
#5593=SURFACE_STYLE_USAGE(.BOTH.,#5607);
#5607=SURFACE_SIDE_STYLE('',(#5621));
#5621=SURFACE_STYLE_FILL_AREA(#5635);
#5635=FILL_AREA_STYLE('',(#5649));
#5649=FILL_AREA_STYLE_COLOUR('',#5657);
#5657=COLOUR_RGB('', 0.66274510, 0.83137255, 0.94901961);
#5670=MANIFOLD_SOLID_BREP('Part 1',#5551);
#5686=SHAPE_DEFINITION_REPRESENTATION(#10206,#5702);
#5702=SHAPE_REPRESENTATION('Part 1',(#5704),#10156);
#5704=AXIS2_PLACEMENT_3D('',#8391,#6505,#6506);
#6451=AXIS2_PLACEMENT_3D('',#9989,#8258,#8259);
#6452=AXIS2_PLACEMENT_3D('',#9990,#8260,#8261);
#6453=AXIS2_PLACEMENT_3D('',#9993,#8262,#8263);
#6454=AXIS2_PLACEMENT_3D('',#9997,#8265,#8266);
#6455=AXIS2_PLACEMENT_3D('',#10003,#8269,#8270);
#6456=AXIS2_PLACEMENT_3D('',#10007,#8272,#8273);
#6457=AXIS2_PLACEMENT_3D('',#10009,#8274,#8275);
#6458=AXIS2_PLACEMENT_3D('',#10012,#8277,#8278);
#6459=AXIS2_PLACEMENT_3D('',#10014,#8279,#8280);
#6460=AXIS2_PLACEMENT_3D('',#10015,#8281,#8282);
#6461=AXIS2_PLACEMENT_3D('',#10020,#8284,#8285);
#6462=AXIS2_PLACEMENT_3D('',#10022,#8286,#8287);
#6463=AXIS2_PLACEMENT_3D('',#10026,#8289,#8290);
#6464=AXIS2_PLACEMENT_3D('',#10032,#8293,#8294);
#6465=AXIS2_PLACEMENT_3D('',#10036,#8296,#8297);
#6466=AXIS2_PLACEMENT_3D('',#10037,#8298,#8299);
#6467=AXIS2_PLACEMENT_3D('',#10039,#8300,#8301);
#6468=AXIS2_PLACEMENT_3D('',#10042,#8304,#8305);
#6469=AXIS2_PLACEMENT_3D('',#10044,#8307,#8308);
#6470=AXIS2_PLACEMENT_3D('',#10046,#8310,#8311);
#6471=AXIS2_PLACEMENT_3D('',#10048,#8313,#8314);
#6472=AXIS2_PLACEMENT_3D('',#10050,#8316,#8317);
#6473=AXIS2_PLACEMENT_3D('',#10052,#8319,#8320);
#6474=AXIS2_PLACEMENT_3D('',#10054,#8322,#8323);
#6475=AXIS2_PLACEMENT_3D('',#10056,#8325,#8326);
#6476=AXIS2_PLACEMENT_3D('',#10058,#8328,#8329);
#6477=AXIS2_PLACEMENT_3D('',#10060,#8331,#8332);
#6478=AXIS2_PLACEMENT_3D('',#10061,#8333,#8334);
#6505=DIRECTION('',(0.,0.,1.));
#6506=DIRECTION('',(1.,0.,0.));
#8258=DIRECTION('',(0.,1.,0.));
#8259=DIRECTION('',(0.,0.,1.));
#8260=DIRECTION('',(0.,1.,0.));
#8261=DIRECTION('',(0.,0.,1.));
#8262=DIRECTION('',(0.,-1.,0.));
#8263=DIRECTION('',(0.,0.,1.));
#8264=DIRECTION('',(-0.034645075969331,0.,-0.999399679162986));
#8265=DIRECTION('',(0.,1.,0.));
#8266=DIRECTION('',(0.,0.,1.));
#8267=DIRECTION('',(-0.0346450759693315,0.,-0.999399679162986));
#8268=DIRECTION('',(-0.0346450759693315,0.,0.999399679162986));
#8269=DIRECTION('',(0.,1.,0.));
#8270=DIRECTION('',(0.,0.,1.));
#8271=DIRECTION('',(-0.034645075969331,0.,0.999399679162986));
#8272=DIRECTION('',(0.,-1.,0.));
#8273=DIRECTION('',(0.,0.,-1.));
#8274=DIRECTION('',(0.,1.,0.));
#8275=DIRECTION('',(0.,0.,-1.));
#8276=DIRECTION('',(1.,0.,0.));
#8277=DIRECTION('',(0.,1.,0.));
#8278=DIRECTION('',(0.,0.,1.));
#8279=DIRECTION('',(0.,1.,0.));
#8280=DIRECTION('',(0.,0.,1.));
#8281=DIRECTION('',(0.,1.,0.));
#8282=DIRECTION('',(0.,0.,1.));
#8283=DIRECTION('',(1.,0.,0.));
#8284=DIRECTION('',(0.,1.,0.));
#8285=DIRECTION('',(0.,0.,-1.));
#8286=DIRECTION('',(0.,-1.,0.));
#8287=DIRECTION('',(0.,0.,-1.));
#8288=DIRECTION('',(-0.034645075969331,0.,0.999399679162986));
#8289=DIRECTION('',(0.,1.,0.));
#8290=DIRECTION('',(0.,0.,1.));
#8291=DIRECTION('',(-0.0346450759693315,0.,0.999399679162986));
#8292=DIRECTION('',(-0.0346450759693315,0.,-0.999399679162986));
#8293=DIRECTION('',(0.,1.,0.));
#8294=DIRECTION('',(0.,0.,1.));
#8295=DIRECTION('',(-0.034645075969331,0.,-0.999399679162986));
#8296=DIRECTION('',(0.,-1.,0.));
#8297=DIRECTION('',(0.,0.,1.));
#8298=DIRECTION('',(0.,1.,0.));
#8299=DIRECTION('',(0.,0.,1.));
#8300=DIRECTION('',(0.,-1.,0.));
#8301=DIRECTION('',(0.,0.,-1.));
#8302=DIRECTION('',(0.,-1.,0.));
#8303=DIRECTION('',(0.,-1.,0.));
#8304=DIRECTION('',(0.,-1.,0.));
#8305=DIRECTION('',(0.,0.,-1.));
#8306=DIRECTION('',(0.,-1.,0.));
#8307=DIRECTION('',(-0.999399679162986,0.,0.034645075969331));
#8308=DIRECTION('',(0.034645075969331,0.,0.999399679162986));
#8309=DIRECTION('',(0.,-1.,0.));
#8310=DIRECTION('',(0.,-1.,0.));
#8311=DIRECTION('',(0.,0.,-1.));
#8312=DIRECTION('',(0.,-1.,0.));
#8313=DIRECTION('',(-0.999399679162986,0.,0.0346450759693315));
#8314=DIRECTION('',(0.0346450759693315,0.,0.999399679162986));
#8315=DIRECTION('',(0.,-1.,0.));
#8316=DIRECTION('',(0.999399679162986,0.,0.0346450759693315));
#8317=DIRECTION('',(0.0346450759693315,0.,-0.999399679162986));
#8318=DIRECTION('',(0.,-1.,0.));
#8319=DIRECTION('',(0.,-1.,0.));
#8320=DIRECTION('',(0.,0.,-1.));
#8321=DIRECTION('',(0.,-1.,0.));
#8322=DIRECTION('',(0.999399679162986,0.,0.034645075969331));
#8323=DIRECTION('',(0.034645075969331,0.,-0.999399679162986));
#8324=DIRECTION('',(0.,-1.,0.));
#8325=DIRECTION('',(0.,-1.,0.));
#8326=DIRECTION('',(0.,0.,-1.));
#8327=DIRECTION('',(0.,-1.,0.));
#8328=DIRECTION('',(0.,-1.,0.));
#8329=DIRECTION('',(0.,0.,-1.));
#8330=DIRECTION('',(0.,-1.,0.));
#8331=DIRECTION('',(0.,0.,-1.));
#8332=DIRECTION('',(-1.,0.,0.));
#8333=DIRECTION('',(0.,-1.,0.));
#8334=DIRECTION('',(0.,0.,-1.));
#8391=CARTESIAN_POINT('',(0.,0.,0.));
#9989=CARTESIAN_POINT('',(0.00569655549855441,0.0005,-0.000257682665739804));
#9990=CARTESIAN_POINT('',(0.00569655549855441,0.0005,-0.000257682665739804));
#9991=CARTESIAN_POINT('',(0.00569655549855441,0.0005,0.));
#9992=CARTESIAN_POINT('',(0.00581839809795156,0.0005,-0.000484739348519487));
#9993=CARTESIAN_POINT('',(0.00938954980005402,0.0005,-0.00713966843895529));
#9994=CARTESIAN_POINT('',(0.00184152090594629,0.0005,-0.00687800932508196));
#9995=CARTESIAN_POINT('',(0.00182205353244363,0.0005,-0.00743958081217945));
#9996=CARTESIAN_POINT('',(0.00182205353244363,0.0005,-0.00743958081217945));
#9997=CARTESIAN_POINT('',(0.,0.0005,-0.00915134041122065));
#9998=CARTESIAN_POINT('',(0.00169914269912228,0.0005,-0.0109851653996041));
#9999=CARTESIAN_POINT('',(0.,0.0005,-0.06));
#10000=CARTESIAN_POINT('',(0.,0.0005,-0.06));
#10001=CARTESIAN_POINT('',(0.,0.0005,-0.06));
#10002=CARTESIAN_POINT('',(-0.00169914269912228,0.0005,-0.0109851653996041));
#10003=CARTESIAN_POINT('',(0.,0.0005,-0.00915134041122065));
#10004=CARTESIAN_POINT('',(-0.00182205353244363,0.0005,-0.00743958081217945));
#10005=CARTESIAN_POINT('',(-0.00182205353244363,0.0005,-0.00743958081217945));
#10006=CARTESIAN_POINT('',(-0.0018415209059463,0.0005,-0.00687800932508196));
#10007=CARTESIAN_POINT('',(-0.00938954980005402,0.0005,-0.00713966843895529));
#10008=CARTESIAN_POINT('',(-0.00581839809795156,0.0005,-0.000484739348519492));
#10009=CARTESIAN_POINT('',(-0.00569655549855441,0.0005,-0.000257682665739804));
#10010=CARTESIAN_POINT('',(-0.00569655549855441,0.0005,0.));
#10011=CARTESIAN_POINT('',(-0.00569655549855441,0.0005,0.));
#10012=CARTESIAN_POINT('',(0.,0.0005,-0.00915134041122065));
#10013=CARTESIAN_POINT('',(0.,0.0005,-0.00765134041122065));
#10014=CARTESIAN_POINT('',(0.00569655549855441,0.,-0.000257682665739804));
#10015=CARTESIAN_POINT('',(0.00569655549855441,0.,-0.000257682665739804));
#10016=CARTESIAN_POINT('',(0.00569655549855441,0.,0.));
#10017=CARTESIAN_POINT('',(0.00581839809795156,0.,-0.000484739348519487));
#10018=CARTESIAN_POINT('',(-0.00569655549855441,0.,0.));
#10019=CARTESIAN_POINT('',(-0.00569655549855441,0.,0.));
#10020=CARTESIAN_POINT('',(-0.00569655549855441,0.,-0.000257682665739804));
#10021=CARTESIAN_POINT('',(-0.00581839809795156,0.,-0.000484739348519492));
#10022=CARTESIAN_POINT('',(-0.00938954980005402,0.,-0.00713966843895529));
#10023=CARTESIAN_POINT('',(-0.0018415209059463,0.,-0.00687800932508196));
#10024=CARTESIAN_POINT('',(-0.00182205353244363,0.,-0.00743958081217945));
#10025=CARTESIAN_POINT('',(-0.00182205353244363,0.,-0.00743958081217945));
#10026=CARTESIAN_POINT('',(0.,0.,-0.00915134041122065));
#10027=CARTESIAN_POINT('',(-0.00169914269912228,0.,-0.0109851653996041));
#10028=CARTESIAN_POINT('',(0.,0.,-0.06));
#10029=CARTESIAN_POINT('',(0.,0.,-0.06));
#10030=CARTESIAN_POINT('',(0.,0.,-0.06));
#10031=CARTESIAN_POINT('',(0.00169914269912228,0.,-0.0109851653996041));
#10032=CARTESIAN_POINT('',(0.,0.,-0.00915134041122065));
#10033=CARTESIAN_POINT('',(0.00182205353244363,0.,-0.00743958081217945));
#10034=CARTESIAN_POINT('',(0.00182205353244363,0.,-0.00743958081217945));
#10035=CARTESIAN_POINT('',(0.00184152090594629,0.,-0.00687800932508196));
#10036=CARTESIAN_POINT('',(0.00938954980005402,0.,-0.00713966843895529));
#10037=CARTESIAN_POINT('',(0.,0.,-0.00915134041122065));
#10038=CARTESIAN_POINT('',(0.,0.,-0.00765134041122065));
#10039=CARTESIAN_POINT('',(0.00569655549855441,0.0005,-0.000257682665739804));
#10040=CARTESIAN_POINT('',(0.00581839809795156,0.0005,-0.000484739348519487));
#10041=CARTESIAN_POINT('',(0.00569655549855441,0.0005,0.));
#10042=CARTESIAN_POINT('',(0.00938954980005402,0.0005,-0.00713966843895529));
#10043=CARTESIAN_POINT('',(0.00184152090594629,0.0005,-0.00687800932508196));
#10044=CARTESIAN_POINT('',(0.00182205353244363,0.0005,-0.00743958081217945));
#10045=CARTESIAN_POINT('',(0.00182205353244363,0.0005,-0.00743958081217945));
#10046=CARTESIAN_POINT('',(0.,0.0005,-0.00915134041122065));
#10047=CARTESIAN_POINT('',(0.00169914269912228,0.0005,-0.0109851653996041));
#10048=CARTESIAN_POINT('',(0.,0.0005,-0.06));
#10049=CARTESIAN_POINT('',(0.,0.0005,-0.06));
#10050=CARTESIAN_POINT('',(0.,0.0005,-0.06));
#10051=CARTESIAN_POINT('',(-0.00169914269912228,0.0005,-0.0109851653996041));
#10052=CARTESIAN_POINT('',(0.,0.0005,-0.00915134041122065));
#10053=CARTESIAN_POINT('',(-0.00182205353244363,0.0005,-0.00743958081217945));
#10054=CARTESIAN_POINT('',(-0.00182205353244363,0.0005,-0.00743958081217945));
#10055=CARTESIAN_POINT('',(-0.0018415209059463,0.0005,-0.00687800932508196));
#10056=CARTESIAN_POINT('',(-0.00938954980005402,0.0005,-0.00713966843895529));
#10057=CARTESIAN_POINT('',(-0.00581839809795156,0.0005,-0.000484739348519492));
#10058=CARTESIAN_POINT('',(-0.00569655549855441,0.0005,-0.000257682665739804));
#10059=CARTESIAN_POINT('',(-0.00569655549855441,0.0005,0.));
#10060=CARTESIAN_POINT('',(-0.00569655549855441,0.0005,0.));
#10061=CARTESIAN_POINT('',(0.,0.0005,-0.00915134041122065));
#10141=MECHANICAL_DESIGN_GEOMETRIC_PRESENTATION_REPRESENTATION('',(#5565),#10142);
#10142=(
GEOMETRIC_REPRESENTATION_CONTEXT(3)
GLOBAL_UNCERTAINTY_ASSIGNED_CONTEXT((#10158))
GLOBAL_UNIT_ASSIGNED_CONTEXT((#10176,#10175,#10174))
REPRESENTATION_CONTEXT('MAS-674','TOP_LEVEL_ASSEMBLY_PART')
);
#10156=(
GEOMETRIC_REPRESENTATION_CONTEXT(3)
GLOBAL_UNCERTAINTY_ASSIGNED_CONTEXT((#10172))
GLOBAL_UNIT_ASSIGNED_CONTEXT((#10176,#10175,#10174))
REPRESENTATION_CONTEXT('Part 1','COMPONENT_PART')
);
#10158=UNCERTAINTY_MEASURE_WITH_UNIT(LENGTH_MEASURE(1.E-8),#10176,
'DISTANCE_ACCURACY_VALUE','Maximum Tolerance applied to model');
#10172=UNCERTAINTY_MEASURE_WITH_UNIT(LENGTH_MEASURE(1.E-8),#10176,
'DISTANCE_ACCURACY_VALUE','Maximum Tolerance applied to model');
#10174=(
NAMED_UNIT(*)
SI_UNIT($,.STERADIAN.)
SOLID_ANGLE_UNIT()
);
#10175=(
NAMED_UNIT(*)
PLANE_ANGLE_UNIT()
SI_UNIT($,.RADIAN.)
);
#10176=(
LENGTH_UNIT()
NAMED_UNIT(*)
SI_UNIT($,.METRE.)
);
#10206=PRODUCT_DEFINITION_SHAPE('','',#10224);
#10224=PRODUCT_DEFINITION('','',#10256,#10240);
#10240=PRODUCT_DEFINITION_CONTEXT('',#10323,'design');
#10256=PRODUCT_DEFINITION_FORMATION_WITH_SPECIFIED_SOURCE('','',#10288,
 .NOT_KNOWN.);
#10288=PRODUCT('Part 1','Part 1','Part 1',(#10320));
#10320=PRODUCT_CONTEXT('',#10323,'mechanical');
#10323=APPLICATION_CONTEXT('managed model based 3d engineering');
ENDSEC;
END-ISO-10303-21;
